ISO-10303-21;
HEADER;
/* Generated by software containing ST-Developer
 * from STEP Tools, Inc. (www.steptools.com) 
 */

FILE_DESCRIPTION(
/* description */ ('Lever-operated bar clamp (toggle)'),
/* implementation_level */ '2;1');

FILE_NAME(
/* name */ 'Foot strip (1).step',
/* time_stamp */ '2026-10-28T03:25:02-07:00',
/* author */ (''),
/* organization */ (''),
/* preprocessor_version */ 'ST-DEVELOPER v20.2',
/* originating_system */ 'Autodesk Translation Framework v15.17.0.0',
/* authorisation */ '');

FILE_SCHEMA (('AUTOMOTIVE_DESIGN { 1 0 10303 214 3 1 1 }'));
ENDSEC;

DATA;
#10=MECHANICAL_DESIGN_GEOMETRIC_PRESENTATION_REPRESENTATION('',(#412),#12413);
#336=SHAPE_REPRESENTATION_RELATIONSHIP('SRR','None',#12575,#374);
#374=ADVANCED_BREP_SHAPE_REPRESENTATION('',(#459),#12372);
#412=STYLED_ITEM('',(#12855),#459);
#459=MANIFOLD_SOLID_BREP('Body1',#6571);
#663=PLANE('',#7080);
#664=PLANE('',#7081);
#665=PLANE('',#7082);
#666=PLANE('',#7083);
#667=PLANE('',#7084);
#668=PLANE('',#7085);
#908=FACE_OUTER_BOUND('',#1330,.T.);
#909=FACE_OUTER_BOUND('',#1331,.T.);
#910=FACE_OUTER_BOUND('',#1332,.T.);
#911=FACE_OUTER_BOUND('',#1333,.T.);
#912=FACE_OUTER_BOUND('',#1334,.T.);
#913=FACE_OUTER_BOUND('',#1335,.T.);
#1330=EDGE_LOOP('',(#4517,#4518,#4519,#4520));
#1331=EDGE_LOOP('',(#4521,#4522,#4523,#4524));
#1332=EDGE_LOOP('',(#4525,#4526,#4527,#4528));
#1333=EDGE_LOOP('',(#4529,#4530,#4531,#4532));
#1334=EDGE_LOOP('',(#4533,#4534,#4535,#4536));
#1335=EDGE_LOOP('',(#4537,#4538,#4539,#4540));
#1883=LINE('',#10153,#2324);
#1884=LINE('',#10155,#2325);
#1885=LINE('',#10157,#2326);
#1886=LINE('',#10158,#2327);
#1887=LINE('',#10161,#2328);
#1888=LINE('',#10163,#2329);
#1889=LINE('',#10164,#2330);
#1890=LINE('',#10167,#2331);
#1891=LINE('',#10169,#2332);
#1892=LINE('',#10170,#2333);
#1893=LINE('',#10172,#2334);
#1894=LINE('',#10173,#2335);
#2324=VECTOR('',#8010,1.);
#2325=VECTOR('',#8011,1.);
#2326=VECTOR('',#8012,1.);
#2327=VECTOR('',#8013,1.);
#2328=VECTOR('',#8016,1.);
#2329=VECTOR('',#8017,1.);
#2330=VECTOR('',#8018,1.);
#2331=VECTOR('',#8021,1.);
#2332=VECTOR('',#8022,1.);
#2333=VECTOR('',#8023,1.);
#2334=VECTOR('',#8026,1.);
#2335=VECTOR('',#8027,1.);
#3106=VERTEX_POINT('',#10151);
#3107=VERTEX_POINT('',#10152);
#3108=VERTEX_POINT('',#10154);
#3109=VERTEX_POINT('',#10156);
#3110=VERTEX_POINT('',#10160);
#3111=VERTEX_POINT('',#10162);
#3112=VERTEX_POINT('',#10166);
#3113=VERTEX_POINT('',#10168);
#3663=EDGE_CURVE('',#3106,#3107,#1883,.T.);
#3664=EDGE_CURVE('',#3107,#3108,#1884,.T.);
#3665=EDGE_CURVE('',#3109,#3108,#1885,.T.);
#3666=EDGE_CURVE('',#3106,#3109,#1886,.T.);
#3667=EDGE_CURVE('',#3110,#3106,#1887,.T.);
#3668=EDGE_CURVE('',#3111,#3109,#1888,.T.);
#3669=EDGE_CURVE('',#3110,#3111,#1889,.T.);
#3670=EDGE_CURVE('',#3112,#3110,#1890,.T.);
#3671=EDGE_CURVE('',#3113,#3111,#1891,.T.);
#3672=EDGE_CURVE('',#3112,#3113,#1892,.T.);
#3673=EDGE_CURVE('',#3107,#3112,#1893,.T.);
#3674=EDGE_CURVE('',#3108,#3113,#1894,.T.);
#4517=ORIENTED_EDGE('',*,*,#3663,.T.);
#4518=ORIENTED_EDGE('',*,*,#3664,.T.);
#4519=ORIENTED_EDGE('',*,*,#3665,.F.);
#4520=ORIENTED_EDGE('',*,*,#3666,.F.);
#4521=ORIENTED_EDGE('',*,*,#3667,.T.);
#4522=ORIENTED_EDGE('',*,*,#3666,.T.);
#4523=ORIENTED_EDGE('',*,*,#3668,.F.);
#4524=ORIENTED_EDGE('',*,*,#3669,.F.);
#4525=ORIENTED_EDGE('',*,*,#3670,.T.);
#4526=ORIENTED_EDGE('',*,*,#3669,.T.);
#4527=ORIENTED_EDGE('',*,*,#3671,.F.);
#4528=ORIENTED_EDGE('',*,*,#3672,.F.);
#4529=ORIENTED_EDGE('',*,*,#3673,.T.);
#4530=ORIENTED_EDGE('',*,*,#3672,.T.);
#4531=ORIENTED_EDGE('',*,*,#3674,.F.);
#4532=ORIENTED_EDGE('',*,*,#3664,.F.);
#4533=ORIENTED_EDGE('',*,*,#3674,.T.);
#4534=ORIENTED_EDGE('',*,*,#3671,.T.);
#4535=ORIENTED_EDGE('',*,*,#3668,.T.);
#4536=ORIENTED_EDGE('',*,*,#3665,.T.);
#4537=ORIENTED_EDGE('',*,*,#3673,.F.);
#4538=ORIENTED_EDGE('',*,*,#3663,.F.);
#4539=ORIENTED_EDGE('',*,*,#3667,.F.);
#4540=ORIENTED_EDGE('',*,*,#3670,.F.);
#6183=ADVANCED_FACE('',(#908),#663,.T.);
#6184=ADVANCED_FACE('',(#909),#664,.T.);
#6185=ADVANCED_FACE('',(#910),#665,.T.);
#6186=ADVANCED_FACE('',(#911),#666,.T.);
#6187=ADVANCED_FACE('',(#912),#667,.T.);
#6188=ADVANCED_FACE('',(#913),#668,.F.);
#6571=CLOSED_SHELL('',(#6183,#6184,#6185,#6186,#6187,#6188));
#7079=AXIS2_PLACEMENT_3D('',#10149,#8006,#8007);
#7080=AXIS2_PLACEMENT_3D('',#10150,#8008,#8009);
#7081=AXIS2_PLACEMENT_3D('',#10159,#8014,#8015);
#7082=AXIS2_PLACEMENT_3D('',#10165,#8019,#8020);
#7083=AXIS2_PLACEMENT_3D('',#10171,#8024,#8025);
#7084=AXIS2_PLACEMENT_3D('',#10174,#8028,#8029);
#7085=AXIS2_PLACEMENT_3D('',#10175,#8030,#8031);
#8006=DIRECTION('axis',(0.,0.,1.));
#8007=DIRECTION('refdir',(1.,0.,0.));
#8008=DIRECTION('center_axis',(0.,1.,0.));
#8009=DIRECTION('ref_axis',(-1.,0.,0.));
#8010=DIRECTION('',(-1.,0.,0.));
#8011=DIRECTION('',(0.,0.,1.));
#8012=DIRECTION('',(-1.,0.,0.));
#8013=DIRECTION('',(0.,0.,1.));
#8014=DIRECTION('center_axis',(1.,0.,0.));
#8015=DIRECTION('ref_axis',(0.,1.,0.));
#8016=DIRECTION('',(0.,1.,0.));
#8017=DIRECTION('',(0.,1.,0.));
#8018=DIRECTION('',(0.,0.,1.));
#8019=DIRECTION('center_axis',(0.,-1.,0.));
#8020=DIRECTION('ref_axis',(1.,0.,0.));
#8021=DIRECTION('',(1.,0.,0.));
#8022=DIRECTION('',(1.,0.,0.));
#8023=DIRECTION('',(0.,0.,1.));
#8024=DIRECTION('center_axis',(-1.,0.,0.));
#8025=DIRECTION('ref_axis',(0.,-1.,0.));
#8026=DIRECTION('',(0.,-1.,0.));
#8027=DIRECTION('',(0.,-1.,0.));
#8028=DIRECTION('center_axis',(0.,0.,1.));
#8029=DIRECTION('ref_axis',(1.,0.,0.));
#8030=DIRECTION('center_axis',(0.,0.,1.));
#8031=DIRECTION('ref_axis',(1.,0.,0.));
#10149=CARTESIAN_POINT('',(0.,0.,0.));
#10150=CARTESIAN_POINT('Origin',(3.5,4.5,-0.8));
#10151=CARTESIAN_POINT('',(3.5,4.5,-0.8));
#10152=CARTESIAN_POINT('',(-9.5,4.5,-0.8));
#10153=CARTESIAN_POINT('',(3.5,4.5,-0.8));
#10154=CARTESIAN_POINT('',(-9.5,4.5,0.));
#10155=CARTESIAN_POINT('',(-9.5,4.5,-0.8));
#10156=CARTESIAN_POINT('',(3.5,4.5,0.));
#10157=CARTESIAN_POINT('',(3.5,4.5,0.));
#10158=CARTESIAN_POINT('',(3.5,4.5,-0.8));
#10159=CARTESIAN_POINT('Origin',(3.5,3.7,-0.8));
#10160=CARTESIAN_POINT('',(3.5,3.7,-0.8));
#10161=CARTESIAN_POINT('',(3.5,3.7,-0.8));
#10162=CARTESIAN_POINT('',(3.5,3.7,0.));
#10163=CARTESIAN_POINT('',(3.5,3.7,0.));
#10164=CARTESIAN_POINT('',(3.5,3.7,-0.8));
#10165=CARTESIAN_POINT('Origin',(-9.5,3.7,-0.8));
#10166=CARTESIAN_POINT('',(-9.5,3.7,-0.8));
#10167=CARTESIAN_POINT('',(-9.5,3.7,-0.8));
#10168=CARTESIAN_POINT('',(-9.5,3.7,0.));
#10169=CARTESIAN_POINT('',(-9.5,3.7,0.));
#10170=CARTESIAN_POINT('',(-9.5,3.7,-0.8));
#10171=CARTESIAN_POINT('Origin',(-9.5,4.5,-0.8));
#10172=CARTESIAN_POINT('',(-9.5,4.5,-0.8));
#10173=CARTESIAN_POINT('',(-9.5,4.5,0.));
#10174=CARTESIAN_POINT('Origin',(-3.,4.1,0.));
#10175=CARTESIAN_POINT('Origin',(-3.,4.1,-0.8));
#12326=UNCERTAINTY_MEASURE_WITH_UNIT(LENGTH_MEASURE(0.001),#12414,
'DISTANCE_ACCURACY_VALUE',
'Maximum model space distance between geometric entities at asserted c
onnectivities');
#12367=UNCERTAINTY_MEASURE_WITH_UNIT(LENGTH_MEASURE(0.001),#12414,
'DISTANCE_ACCURACY_VALUE',
'Maximum model space distance between geometric entities at asserted c
onnectivities');
#12372=(
GEOMETRIC_REPRESENTATION_CONTEXT(3)
GLOBAL_UNCERTAINTY_ASSIGNED_CONTEXT((#12326))
GLOBAL_UNIT_ASSIGNED_CONTEXT((#12414,#12416,#12417))
REPRESENTATION_CONTEXT('','3D')
);
#12413=(
GEOMETRIC_REPRESENTATION_CONTEXT(3)
GLOBAL_UNCERTAINTY_ASSIGNED_CONTEXT((#12367))
GLOBAL_UNIT_ASSIGNED_CONTEXT((#12414,#12416,#12417))
REPRESENTATION_CONTEXT('','3D')
);
#12414=(
LENGTH_UNIT()
NAMED_UNIT(*)
SI_UNIT(.CENTI.,.METRE.)
);
#12416=(
NAMED_UNIT(*)
PLANE_ANGLE_UNIT()
SI_UNIT($,.RADIAN.)
);
#12417=(
NAMED_UNIT(*)
SI_UNIT($,.STERADIAN.)
SOLID_ANGLE_UNIT()
);
#12422=SHAPE_DEFINITION_REPRESENTATION(#12467,#12575);
#12467=PRODUCT_DEFINITION_SHAPE('',$,#12621);
#12575=SHAPE_REPRESENTATION('',(#7079),#12372);
#12616=PRODUCT_DEFINITION_CONTEXT('part definition',#12753,'design');
#12621=PRODUCT_DEFINITION('Foot strip (1)','Foot strip (1)',#12666,#12616);
#12666=PRODUCT_DEFINITION_FORMATION('',$,#12759);
#12753=APPLICATION_CONTEXT(
'Core Data for Automotive Mechanical Design Process');
#12754=PRODUCT_CONTEXT('part definition',#12753,'mechanical');
#12759=PRODUCT('Foot strip (1)','Foot strip (1)','Foot strip (1)',(#12754));
#12849=COLOUR_RGB('Light Blue',0.38,0.62,0.78);
#12850=FILL_AREA_STYLE_COLOUR('',#12849);
#12851=FILL_AREA_STYLE('',(#12850));
#12852=SURFACE_STYLE_FILL_AREA(#12851);
#12853=SURFACE_SIDE_STYLE('',(#12852));
#12854=SURFACE_STYLE_USAGE(.BOTH.,#12853);
#12855=PRESENTATION_STYLE_ASSIGNMENT((#12854));
ENDSEC;
END-ISO-10303-21;
